ISO-10303-21;
HEADER;
/* Generated by software containing ST-Developer
 * from STEP Tools, Inc. (www.steptools.com) 
 */

FILE_DESCRIPTION(
/* description */ (''),
/* implementation_level */ '2;1');

FILE_NAME(
/* name */ 'Back_Block.step',
/* time_stamp */ '2026-10-19T01:17:59+06:00',
/* author */ (''),
/* organization */ (''),
/* preprocessor_version */ 'ST-DEVELOPER v20.2',
/* originating_system */ 'Autodesk Translation Framework v15.15.0.0',
/* authorisation */ '');

FILE_SCHEMA (('AUTOMOTIVE_DESIGN { 1 0 10303 214 3 1 1 }'));
ENDSEC;

DATA;
#10=MECHANICAL_DESIGN_GEOMETRIC_PRESENTATION_REPRESENTATION('',(#752),#48369);
#621=SHAPE_REPRESENTATION_RELATIONSHIP('SRR','None',#48421,#632);
#632=ADVANCED_BREP_SHAPE_REPRESENTATION('',(#778),#48366);
#725=FACE_BOUND('',#3341,.T.);
#726=FACE_BOUND('',#3343,.T.);
#752=STYLED_ITEM('',(#48496),#778);
#778=MANIFOLD_SOLID_BREP('Back_Block',#20131);
#1187=CYLINDRICAL_SURFACE('',#21820,5.);
#2201=FACE_OUTER_BOUND('',#3335,.T.);
#2202=FACE_OUTER_BOUND('',#3336,.T.);
#2203=FACE_OUTER_BOUND('',#3337,.T.);
#2204=FACE_OUTER_BOUND('',#3338,.T.);
#2205=FACE_OUTER_BOUND('',#3339,.T.);
#2206=FACE_OUTER_BOUND('',#3340,.T.);
#2207=FACE_OUTER_BOUND('',#3342,.T.);
#3335=EDGE_LOOP('',(#18271,#18272,#18273,#18274));
#3336=EDGE_LOOP('',(#18275,#18276,#18277,#18278));
#3337=EDGE_LOOP('',(#18279,#18280,#18281,#18282));
#3338=EDGE_LOOP('',(#18283,#18284,#18285,#18286));
#3339=EDGE_LOOP('',(#18287,#18288,#18289,#18290));
#3340=EDGE_LOOP('',(#18291,#18292,#18293,#18294));
#3341=EDGE_LOOP('',(#18295));
#3342=EDGE_LOOP('',(#18296,#18297,#18298,#18299));
#3343=EDGE_LOOP('',(#18300));
#3953=CIRCLE('',#21821,5.);
#3954=CIRCLE('',#21822,5.);
#5782=LINE('',#48062,#7663);
#5783=LINE('',#48067,#7664);
#5784=LINE('',#48069,#7665);
#5785=LINE('',#48071,#7666);
#5786=LINE('',#48072,#7667);
#5787=LINE('',#48075,#7668);
#5788=LINE('',#48077,#7669);
#5789=LINE('',#48078,#7670);
#5790=LINE('',#48081,#7671);
#5791=LINE('',#48083,#7672);
#5792=LINE('',#48084,#7673);
#5793=LINE('',#48086,#7674);
#5794=LINE('',#48087,#7675);
#7663=VECTOR('',#26847,20.);
#7664=VECTOR('',#26852,10.);
#7665=VECTOR('',#26853,10.);
#7666=VECTOR('',#26854,10.);
#7667=VECTOR('',#26855,10.);
#7668=VECTOR('',#26858,10.);
#7669=VECTOR('',#26859,10.);
#7670=VECTOR('',#26860,10.);
#7671=VECTOR('',#26863,10.);
#7672=VECTOR('',#26864,10.);
#7673=VECTOR('',#26865,10.);
#7674=VECTOR('',#26868,10.);
#7675=VECTOR('',#26869,10.);
#9621=VERTEX_POINT('',#48059);
#9622=VERTEX_POINT('',#48061);
#9623=VERTEX_POINT('',#48065);
#9624=VERTEX_POINT('',#48066);
#9625=VERTEX_POINT('',#48068);
#9626=VERTEX_POINT('',#48070);
#9627=VERTEX_POINT('',#48074);
#9628=VERTEX_POINT('',#48076);
#9629=VERTEX_POINT('',#48080);
#9630=VERTEX_POINT('',#48082);
#12519=EDGE_CURVE('',#9621,#9621,#3953,.T.);
#12520=EDGE_CURVE('',#9621,#9622,#5782,.T.);
#12521=EDGE_CURVE('',#9622,#9622,#3954,.F.);
#12522=EDGE_CURVE('',#9623,#9624,#5783,.T.);
#12523=EDGE_CURVE('',#9623,#9625,#5784,.F.);
#12524=EDGE_CURVE('',#9626,#9625,#5785,.T.);
#12525=EDGE_CURVE('',#9624,#9626,#5786,.T.);
#12526=EDGE_CURVE('',#9624,#9627,#5787,.T.);
#12527=EDGE_CURVE('',#9628,#9626,#5788,.T.);
#12528=EDGE_CURVE('',#9627,#9628,#5789,.T.);
#12529=EDGE_CURVE('',#9627,#9629,#5790,.T.);
#12530=EDGE_CURVE('',#9630,#9628,#5791,.T.);
#12531=EDGE_CURVE('',#9629,#9630,#5792,.T.);
#12532=EDGE_CURVE('',#9629,#9623,#5793,.T.);
#12533=EDGE_CURVE('',#9625,#9630,#5794,.F.);
#18271=ORIENTED_EDGE('',*,*,#12519,.F.);
#18272=ORIENTED_EDGE('',*,*,#12520,.T.);
#18273=ORIENTED_EDGE('',*,*,#12521,.F.);
#18274=ORIENTED_EDGE('',*,*,#12520,.F.);
#18275=ORIENTED_EDGE('',*,*,#12522,.F.);
#18276=ORIENTED_EDGE('',*,*,#12523,.T.);
#18277=ORIENTED_EDGE('',*,*,#12524,.F.);
#18278=ORIENTED_EDGE('',*,*,#12525,.F.);
#18279=ORIENTED_EDGE('',*,*,#12526,.F.);
#18280=ORIENTED_EDGE('',*,*,#12525,.T.);
#18281=ORIENTED_EDGE('',*,*,#12527,.F.);
#18282=ORIENTED_EDGE('',*,*,#12528,.F.);
#18283=ORIENTED_EDGE('',*,*,#12529,.F.);
#18284=ORIENTED_EDGE('',*,*,#12528,.T.);
#18285=ORIENTED_EDGE('',*,*,#12530,.F.);
#18286=ORIENTED_EDGE('',*,*,#12531,.F.);
#18287=ORIENTED_EDGE('',*,*,#12532,.F.);
#18288=ORIENTED_EDGE('',*,*,#12531,.T.);
#18289=ORIENTED_EDGE('',*,*,#12533,.F.);
#18290=ORIENTED_EDGE('',*,*,#12523,.F.);
#18291=ORIENTED_EDGE('',*,*,#12533,.T.);
#18292=ORIENTED_EDGE('',*,*,#12530,.T.);
#18293=ORIENTED_EDGE('',*,*,#12527,.T.);
#18294=ORIENTED_EDGE('',*,*,#12524,.T.);
#18295=ORIENTED_EDGE('',*,*,#12519,.T.);
#18296=ORIENTED_EDGE('',*,*,#12532,.T.);
#18297=ORIENTED_EDGE('',*,*,#12522,.T.);
#18298=ORIENTED_EDGE('',*,*,#12526,.T.);
#18299=ORIENTED_EDGE('',*,*,#12529,.T.);
#18300=ORIENTED_EDGE('',*,*,#12521,.T.);
#19034=PLANE('',#21823);
#19035=PLANE('',#21824);
#19036=PLANE('',#21825);
#19037=PLANE('',#21826);
#19038=PLANE('',#21827);
#19039=PLANE('',#21828);
#20058=ADVANCED_FACE('',(#2201),#1187,.F.);
#20059=ADVANCED_FACE('',(#2202),#19034,.T.);
#20060=ADVANCED_FACE('',(#2203),#19035,.T.);
#20061=ADVANCED_FACE('',(#2204),#19036,.T.);
#20062=ADVANCED_FACE('',(#2205),#19037,.T.);
#20063=ADVANCED_FACE('',(#2206,#725),#19038,.T.);
#20064=ADVANCED_FACE('',(#2207,#726),#19039,.F.);
#20131=CLOSED_SHELL('',(#20058,#20059,#20060,#20061,#20062,#20063,#20064));
#21819=AXIS2_PLACEMENT_3D('',#48057,#26841,#26842);
#21820=AXIS2_PLACEMENT_3D('',#48058,#26843,#26844);
#21821=AXIS2_PLACEMENT_3D('',#48060,#26845,#26846);
#21822=AXIS2_PLACEMENT_3D('',#48063,#26848,#26849);
#21823=AXIS2_PLACEMENT_3D('',#48064,#26850,#26851);
#21824=AXIS2_PLACEMENT_3D('',#48073,#26856,#26857);
#21825=AXIS2_PLACEMENT_3D('',#48079,#26861,#26862);
#21826=AXIS2_PLACEMENT_3D('',#48085,#26866,#26867);
#21827=AXIS2_PLACEMENT_3D('',#48088,#26870,#26871);
#21828=AXIS2_PLACEMENT_3D('',#48089,#26872,#26873);
#26841=DIRECTION('axis',(0.,0.,1.));
#26842=DIRECTION('refdir',(1.,0.,0.));
#26843=DIRECTION('center_axis',(0.,-1.,0.));
#26844=DIRECTION('ref_axis',(-1.,0.,0.));
#26845=DIRECTION('center_axis',(0.,-1.,0.));
#26846=DIRECTION('ref_axis',(-1.,0.,0.));
#26847=DIRECTION('',(0.,-1.,0.));
#26848=DIRECTION('center_axis',(0.,-1.,0.));
#26849=DIRECTION('ref_axis',(-1.,0.,0.));
#26850=DIRECTION('center_axis',(-1.,0.,0.));
#26851=DIRECTION('ref_axis',(0.,0.,1.));
#26852=DIRECTION('',(0.,0.,-1.));
#26853=DIRECTION('',(0.,-1.,0.));
#26854=DIRECTION('',(0.,0.,1.));
#26855=DIRECTION('',(0.,1.,0.));
#26856=DIRECTION('center_axis',(0.,0.,-1.));
#26857=DIRECTION('ref_axis',(-1.,0.,0.));
#26858=DIRECTION('',(1.,0.,0.));
#26859=DIRECTION('',(-1.,0.,0.));
#26860=DIRECTION('',(0.,1.,0.));
#26861=DIRECTION('center_axis',(1.,0.,0.));
#26862=DIRECTION('ref_axis',(0.,0.,-1.));
#26863=DIRECTION('',(0.,0.,1.));
#26864=DIRECTION('',(0.,0.,-1.));
#26865=DIRECTION('',(0.,1.,0.));
#26866=DIRECTION('center_axis',(0.,0.,1.));
#26867=DIRECTION('ref_axis',(1.,0.,0.));
#26868=DIRECTION('',(-1.,0.,0.));
#26869=DIRECTION('',(-1.,0.,0.));
#26870=DIRECTION('center_axis',(0.,1.,0.));
#26871=DIRECTION('ref_axis',(0.,0.,1.));
#26872=DIRECTION('center_axis',(0.,1.,0.));
#26873=DIRECTION('ref_axis',(1.,0.,0.));
#48057=CARTESIAN_POINT('',(0.,0.,0.));
#48058=CARTESIAN_POINT('Origin',(74.9879498948689,510.,53.0228109606356));
#48059=CARTESIAN_POINT('',(79.9879498948689,510.,53.0228109606356));
#48060=CARTESIAN_POINT('Origin',(74.9879498948689,510.,53.0228109606356));
#48061=CARTESIAN_POINT('',(79.9879498948689,495.,53.0228109606356));
#48062=CARTESIAN_POINT('',(79.9879498948689,510.,53.0228109606356));
#48063=CARTESIAN_POINT('Origin',(74.9879498948689,495.,53.0228109606356));
#48064=CARTESIAN_POINT('Origin',(0.,495.,0.));
#48065=CARTESIAN_POINT('',(0.,495.,95.));
#48066=CARTESIAN_POINT('',(0.,495.,0.));
#48067=CARTESIAN_POINT('',(0.,495.,85.));
#48068=CARTESIAN_POINT('',(0.,510.,95.));
#48069=CARTESIAN_POINT('',(0.,495.,95.));
#48070=CARTESIAN_POINT('',(0.,510.,0.));
#48071=CARTESIAN_POINT('',(0.,510.,85.));
#48072=CARTESIAN_POINT('',(0.,495.,0.));
#48073=CARTESIAN_POINT('Origin',(150.,495.,0.));
#48074=CARTESIAN_POINT('',(150.,495.,0.));
#48075=CARTESIAN_POINT('',(0.,495.,0.));
#48076=CARTESIAN_POINT('',(150.,510.,0.));
#48077=CARTESIAN_POINT('',(0.,510.,0.));
#48078=CARTESIAN_POINT('',(150.,495.,0.));
#48079=CARTESIAN_POINT('Origin',(150.,495.,85.));
#48080=CARTESIAN_POINT('',(150.,495.,95.));
#48081=CARTESIAN_POINT('',(150.,495.,0.));
#48082=CARTESIAN_POINT('',(150.,510.,95.));
#48083=CARTESIAN_POINT('',(150.,510.,0.));
#48084=CARTESIAN_POINT('',(150.,495.,95.));
#48085=CARTESIAN_POINT('Origin',(0.,495.,95.));
#48086=CARTESIAN_POINT('',(37.5,495.,95.));
#48087=CARTESIAN_POINT('',(37.5,510.,95.));
#48088=CARTESIAN_POINT('Origin',(75.,510.,42.5));
#48089=CARTESIAN_POINT('Origin',(75.,495.,42.5));
#48353=UNCERTAINTY_MEASURE_WITH_UNIT(LENGTH_MEASURE(0.01),#48370,
'DISTANCE_ACCURACY_VALUE',
'Maximum model space distance between geometric entities at asserted c
onnectivities');
#48356=UNCERTAINTY_MEASURE_WITH_UNIT(LENGTH_MEASURE(0.01),#48370,
'DISTANCE_ACCURACY_VALUE',
'Maximum model space distance between geometric entities at asserted c
onnectivities');
#48366=(
GEOMETRIC_REPRESENTATION_CONTEXT(3)
GLOBAL_UNCERTAINTY_ASSIGNED_CONTEXT((#48353))
GLOBAL_UNIT_ASSIGNED_CONTEXT((#48370,#48372,#48373))
REPRESENTATION_CONTEXT('','3D')
);
#48369=(
GEOMETRIC_REPRESENTATION_CONTEXT(3)
GLOBAL_UNCERTAINTY_ASSIGNED_CONTEXT((#48356))
GLOBAL_UNIT_ASSIGNED_CONTEXT((#48370,#48372,#48373))
REPRESENTATION_CONTEXT('','3D')
);
#48370=(
LENGTH_UNIT()
NAMED_UNIT(*)
SI_UNIT(.MILLI.,.METRE.)
);
#48372=(
NAMED_UNIT(*)
PLANE_ANGLE_UNIT()
SI_UNIT($,.RADIAN.)
);
#48373=(
NAMED_UNIT(*)
SI_UNIT($,.STERADIAN.)
SOLID_ANGLE_UNIT()
);
#48383=SHAPE_DEFINITION_REPRESENTATION(#48395,#48421);
#48395=PRODUCT_DEFINITION_SHAPE('',$,#48434);
#48421=SHAPE_REPRESENTATION('',(#21819),#48366);
#48424=PRODUCT_DEFINITION_CONTEXT('part definition',#48462,'design');
#48434=PRODUCT_DEFINITION('Back_Block','Back_Block',#48446,#48424);
#48446=PRODUCT_DEFINITION_FORMATION('',$,#48473);
#48462=APPLICATION_CONTEXT(
'Core Data for Automotive Mechanical Design Process');
#48463=PRODUCT_CONTEXT('part definition',#48462,'mechanical');
#48473=PRODUCT('Back_Block','Back_Block',$,(#48463));
#48490=COLOUR_RGB('Dark Blue',0.08,0.2,0.34);
#48491=FILL_AREA_STYLE_COLOUR('',#48490);
#48492=FILL_AREA_STYLE('',(#48491));
#48493=SURFACE_STYLE_FILL_AREA(#48492);
#48494=SURFACE_SIDE_STYLE('',(#48493));
#48495=SURFACE_STYLE_USAGE(.BOTH.,#48494);
#48496=PRESENTATION_STYLE_ASSIGNMENT((#48495));
ENDSEC;
END-ISO-10303-21;
